ISO-10303-21;
HEADER;
/* Generated by software containing ST-Developer
 * from STEP Tools, Inc. (www.steptools.com) 
 */

FILE_DESCRIPTION(
/* description */ ('Torque wrench calibration arm'),
/* implementation_level */ '2;1');

FILE_NAME(
/* name */ 'Hanger bearing retainer (1).step',
/* time_stamp */ '2026-10-28T03:24:52-07:00',
/* author */ (''),
/* organization */ (''),
/* preprocessor_version */ 'ST-DEVELOPER v20.2',
/* originating_system */ 'Autodesk Translation Framework v15.17.0.0',
/* authorisation */ '');

FILE_SCHEMA (('AUTOMOTIVE_DESIGN { 1 0 10303 214 3 1 1 }'));
ENDSEC;

DATA;
#10=MECHANICAL_DESIGN_GEOMETRIC_PRESENTATION_REPRESENTATION('',(#455),#12783);
#372=SHAPE_REPRESENTATION_RELATIONSHIP('SRR','None',#12955,#409);
#409=ADVANCED_BREP_SHAPE_REPRESENTATION('',(#507),#12764);
#455=STYLED_ITEM('',(#13212),#507);
#507=MANIFOLD_SOLID_BREP('Body1',#6526);
#618=FACE_BOUND('',#1615,.T.);
#619=FACE_BOUND('',#1619,.T.);
#620=FACE_BOUND('',#1621,.T.);
#799=PLANE('',#7500);
#800=PLANE('',#7507);
#801=PLANE('',#7508);
#1131=FACE_OUTER_BOUND('',#1613,.T.);
#1132=FACE_OUTER_BOUND('',#1614,.T.);
#1133=FACE_OUTER_BOUND('',#1616,.T.);
#1134=FACE_OUTER_BOUND('',#1617,.T.);
#1135=FACE_OUTER_BOUND('',#1618,.T.);
#1136=FACE_OUTER_BOUND('',#1620,.T.);
#1613=EDGE_LOOP('',(#5443,#5444,#5445,#5446));
#1614=EDGE_LOOP('',(#5447));
#1615=EDGE_LOOP('',(#5448));
#1616=EDGE_LOOP('',(#5449,#5450,#5451,#5452));
#1617=EDGE_LOOP('',(#5453,#5454,#5455,#5456));
#1618=EDGE_LOOP('',(#5457));
#1619=EDGE_LOOP('',(#5458));
#1620=EDGE_LOOP('',(#5459));
#1621=EDGE_LOOP('',(#5460));
#2072=LINE('',#11713,#2487);
#2073=LINE('',#11721,#2488);
#2074=LINE('',#11726,#2489);
#2487=VECTOR('',#9174,1.5);
#2488=VECTOR('',#9185,1.1);
#2489=VECTOR('',#9190,2.);
#2846=CIRCLE('',#7498,1.5);
#2847=CIRCLE('',#7499,1.5);
#2848=CIRCLE('',#7501,1.1);
#2849=CIRCLE('',#7503,1.1);
#2850=CIRCLE('',#7505,2.);
#2851=CIRCLE('',#7506,2.);
#3344=VERTEX_POINT('',#11710);
#3345=VERTEX_POINT('',#11712);
#3346=VERTEX_POINT('',#11716);
#3347=VERTEX_POINT('',#11719);
#3348=VERTEX_POINT('',#11723);
#3349=VERTEX_POINT('',#11725);
#4079=EDGE_CURVE('',#3344,#3344,#2846,.T.);
#4080=EDGE_CURVE('',#3344,#3345,#2072,.T.);
#4081=EDGE_CURVE('',#3345,#3345,#2847,.T.);
#4082=EDGE_CURVE('',#3346,#3346,#2848,.T.);
#4083=EDGE_CURVE('',#3347,#3347,#2849,.T.);
#4084=EDGE_CURVE('',#3347,#3346,#2073,.T.);
#4085=EDGE_CURVE('',#3348,#3348,#2850,.T.);
#4086=EDGE_CURVE('',#3348,#3349,#2074,.T.);
#4087=EDGE_CURVE('',#3349,#3349,#2851,.T.);
#5443=ORIENTED_EDGE('',*,*,#4079,.F.);
#5444=ORIENTED_EDGE('',*,*,#4080,.T.);
#5445=ORIENTED_EDGE('',*,*,#4081,.T.);
#5446=ORIENTED_EDGE('',*,*,#4080,.F.);
#5447=ORIENTED_EDGE('',*,*,#4081,.F.);
#5448=ORIENTED_EDGE('',*,*,#4082,.F.);
#5449=ORIENTED_EDGE('',*,*,#4083,.F.);
#5450=ORIENTED_EDGE('',*,*,#4084,.T.);
#5451=ORIENTED_EDGE('',*,*,#4082,.T.);
#5452=ORIENTED_EDGE('',*,*,#4084,.F.);
#5453=ORIENTED_EDGE('',*,*,#4085,.F.);
#5454=ORIENTED_EDGE('',*,*,#4086,.T.);
#5455=ORIENTED_EDGE('',*,*,#4087,.T.);
#5456=ORIENTED_EDGE('',*,*,#4086,.F.);
#5457=ORIENTED_EDGE('',*,*,#4085,.T.);
#5458=ORIENTED_EDGE('',*,*,#4083,.T.);
#5459=ORIENTED_EDGE('',*,*,#4087,.F.);
#5460=ORIENTED_EDGE('',*,*,#4079,.T.);
#6064=CYLINDRICAL_SURFACE('',#7497,1.5);
#6065=CYLINDRICAL_SURFACE('',#7502,1.1);
#6066=CYLINDRICAL_SURFACE('',#7504,2.);
#6356=ADVANCED_FACE('',(#1131),#6064,.T.);
#6357=ADVANCED_FACE('',(#1132,#618),#799,.F.);
#6358=ADVANCED_FACE('',(#1133),#6065,.F.);
#6359=ADVANCED_FACE('',(#1134),#6066,.T.);
#6360=ADVANCED_FACE('',(#1135,#619),#800,.T.);
#6361=ADVANCED_FACE('',(#1136,#620),#801,.F.);
#6526=CLOSED_SHELL('',(#6356,#6357,#6358,#6359,#6360,#6361));
#7496=AXIS2_PLACEMENT_3D('',#11708,#9168,#9169);
#7497=AXIS2_PLACEMENT_3D('',#11709,#9170,#9171);
#7498=AXIS2_PLACEMENT_3D('',#11711,#9172,#9173);
#7499=AXIS2_PLACEMENT_3D('',#11714,#9175,#9176);
#7500=AXIS2_PLACEMENT_3D('',#11715,#9177,#9178);
#7501=AXIS2_PLACEMENT_3D('',#11717,#9179,#9180);
#7502=AXIS2_PLACEMENT_3D('',#11718,#9181,#9182);
#7503=AXIS2_PLACEMENT_3D('',#11720,#9183,#9184);
#7504=AXIS2_PLACEMENT_3D('',#11722,#9186,#9187);
#7505=AXIS2_PLACEMENT_3D('',#11724,#9188,#9189);
#7506=AXIS2_PLACEMENT_3D('',#11727,#9191,#9192);
#7507=AXIS2_PLACEMENT_3D('',#11728,#9193,#9194);
#7508=AXIS2_PLACEMENT_3D('',#11729,#9195,#9196);
#9168=DIRECTION('axis',(0.,0.,1.));
#9169=DIRECTION('refdir',(1.,0.,0.));
#9170=DIRECTION('center_axis',(0.,1.,0.));
#9171=DIRECTION('ref_axis',(1.,0.,0.));
#9172=DIRECTION('center_axis',(0.,1.,0.));
#9173=DIRECTION('ref_axis',(1.,0.,0.));
#9174=DIRECTION('',(0.,-1.,0.));
#9175=DIRECTION('center_axis',(0.,1.,0.));
#9176=DIRECTION('ref_axis',(1.,0.,0.));
#9177=DIRECTION('center_axis',(0.,1.,0.));
#9178=DIRECTION('ref_axis',(1.,0.,0.));
#9179=DIRECTION('center_axis',(0.,-1.,0.));
#9180=DIRECTION('ref_axis',(1.,0.,0.));
#9181=DIRECTION('center_axis',(0.,1.,0.));
#9182=DIRECTION('ref_axis',(1.,0.,0.));
#9183=DIRECTION('center_axis',(0.,-1.,0.));
#9184=DIRECTION('ref_axis',(1.,0.,0.));
#9185=DIRECTION('',(0.,-1.,0.));
#9186=DIRECTION('center_axis',(0.,1.,0.));
#9187=DIRECTION('ref_axis',(1.,0.,0.));
#9188=DIRECTION('center_axis',(0.,1.,0.));
#9189=DIRECTION('ref_axis',(1.,0.,0.));
#9190=DIRECTION('',(0.,-1.,0.));
#9191=DIRECTION('center_axis',(0.,1.,0.));
#9192=DIRECTION('ref_axis',(1.,0.,0.));
#9193=DIRECTION('center_axis',(0.,1.,0.));
#9194=DIRECTION('ref_axis',(1.,0.,0.));
#9195=DIRECTION('center_axis',(0.,1.,0.));
#9196=DIRECTION('ref_axis',(1.,0.,0.));
#11708=CARTESIAN_POINT('',(0.,0.,0.));
#11709=CARTESIAN_POINT('Origin',(50.,8.95,8.));
#11710=CARTESIAN_POINT('',(48.5,9.,8.));
#11711=CARTESIAN_POINT('Origin',(50.,9.,8.));
#11712=CARTESIAN_POINT('',(48.5,8.95,8.));
#11713=CARTESIAN_POINT('',(48.5,8.95,8.));
#11714=CARTESIAN_POINT('Origin',(50.,8.95,8.));
#11715=CARTESIAN_POINT('Origin',(50.,8.95,8.));
#11716=CARTESIAN_POINT('',(48.9,8.95,8.));
#11717=CARTESIAN_POINT('Origin',(50.,8.95,8.));
#11718=CARTESIAN_POINT('Origin',(50.,9.,8.));
#11719=CARTESIAN_POINT('',(48.9,9.2,8.));
#11720=CARTESIAN_POINT('Origin',(50.,9.2,8.));
#11721=CARTESIAN_POINT('',(48.9,9.,8.));
#11722=CARTESIAN_POINT('Origin',(50.,9.,8.));
#11723=CARTESIAN_POINT('',(48.,9.2,8.));
#11724=CARTESIAN_POINT('Origin',(50.,9.2,8.));
#11725=CARTESIAN_POINT('',(48.,9.,8.));
#11726=CARTESIAN_POINT('',(48.,9.,8.));
#11727=CARTESIAN_POINT('Origin',(50.,9.,8.));
#11728=CARTESIAN_POINT('Origin',(50.,9.2,8.));
#11729=CARTESIAN_POINT('Origin',(50.,9.,8.));
#12720=UNCERTAINTY_MEASURE_WITH_UNIT(LENGTH_MEASURE(0.001),#12784,
'DISTANCE_ACCURACY_VALUE',
'Maximum model space distance between geometric entities at asserted c
onnectivities');
#12739=UNCERTAINTY_MEASURE_WITH_UNIT(LENGTH_MEASURE(0.001),#12784,
'DISTANCE_ACCURACY_VALUE',
'Maximum model space distance between geometric entities at asserted c
onnectivities');
#12764=(
GEOMETRIC_REPRESENTATION_CONTEXT(3)
GLOBAL_UNCERTAINTY_ASSIGNED_CONTEXT((#12720))
GLOBAL_UNIT_ASSIGNED_CONTEXT((#12784,#12786,#12787))
REPRESENTATION_CONTEXT('','3D')
);
#12783=(
GEOMETRIC_REPRESENTATION_CONTEXT(3)
GLOBAL_UNCERTAINTY_ASSIGNED_CONTEXT((#12739))
GLOBAL_UNIT_ASSIGNED_CONTEXT((#12784,#12786,#12787))
REPRESENTATION_CONTEXT('','3D')
);
#12784=(
LENGTH_UNIT()
NAMED_UNIT(*)
SI_UNIT(.CENTI.,.METRE.)
);
#12786=(
NAMED_UNIT(*)
PLANE_ANGLE_UNIT()
SI_UNIT($,.RADIAN.)
);
#12787=(
NAMED_UNIT(*)
SI_UNIT($,.STERADIAN.)
SOLID_ANGLE_UNIT()
);
#12812=SHAPE_DEFINITION_REPRESENTATION(#12881,#12955);
#12881=PRODUCT_DEFINITION_SHAPE('',$,#12999);
#12955=SHAPE_REPRESENTATION('',(#7496),#12764);
#12974=PRODUCT_DEFINITION_CONTEXT('part definition',#13105,'design');
#12999=PRODUCT_DEFINITION('Hanger bearing retainer (1)',
'Hanger bearing retainer (1)',#13042,#12974);
#13042=PRODUCT_DEFINITION_FORMATION('',$,#13131);
#13105=APPLICATION_CONTEXT(
'Core Data for Automotive Mechanical Design Process');
#13106=PRODUCT_CONTEXT('part definition',#13105,'mechanical');
#13131=PRODUCT('Hanger bearing retainer (1)',
'Hanger bearing retainer (1)','Hanger bearing retainer (1)',(#13106));
#13206=COLOUR_RGB('Grey',0.48,0.52,0.57);
#13207=FILL_AREA_STYLE_COLOUR('',#13206);
#13208=FILL_AREA_STYLE('',(#13207));
#13209=SURFACE_STYLE_FILL_AREA(#13208);
#13210=SURFACE_SIDE_STYLE('',(#13209));
#13211=SURFACE_STYLE_USAGE(.BOTH.,#13210);
#13212=PRESENTATION_STYLE_ASSIGNMENT((#13211));
ENDSEC;
END-ISO-10303-21;
